ISO-10303-21;
HEADER;
/* Generated by software containing ST-Developer
 * from STEP Tools, Inc. (www.steptools.com) 
 */

FILE_DESCRIPTION(
/* description */ ('Lifting hook block with sheave'),
/* implementation_level */ '2;1');

FILE_NAME(
/* name */ 'Cap Screw - M8x30.step',
/* time_stamp */ '2026-10-28T03:23:54-07:00',
/* author */ (''),
/* organization */ (''),
/* preprocessor_version */ 'ST-DEVELOPER v20.2',
/* originating_system */ 'Autodesk Translation Framework v15.17.0.0',
/* authorisation */ '');

FILE_SCHEMA (('AUTOMOTIVE_DESIGN { 1 0 10303 214 3 1 1 }'));
ENDSEC;

DATA;
#10=MECHANICAL_DESIGN_GEOMETRIC_PRESENTATION_REPRESENTATION('',(#366),#9391);
#272=CONICAL_SURFACE('',#5539,0.625,0.785398163397448);
#273=CONICAL_SURFACE('',#5543,0.635,0.785398163397449);
#274=CONICAL_SURFACE('',#5547,0.41,0.463647609000806);
#275=CONICAL_SURFACE('',#5551,0.36,0.785398163397448);
#286=ORIENTED_CLOSED_SHELL('',*,#4904,.F.);
#289=BREP_WITH_VOIDS('Body1',#4903,(#286));
#306=SHAPE_REPRESENTATION_RELATIONSHIP('SRR','None',#9537,#336);
#336=ADVANCED_BREP_SHAPE_REPRESENTATION('',(#289),#9372);
#366=STYLED_ITEM('',(#9766),#289);
#575=LINE('',#8221,#863);
#576=LINE('',#8225,#864);
#577=LINE('',#8229,#865);
#578=LINE('',#8236,#866);
#579=LINE('',#8240,#867);
#580=LINE('',#8244,#868);
#581=LINE('',#8249,#869);
#582=LINE('',#8251,#870);
#583=LINE('',#8253,#871);
#584=LINE('',#8254,#872);
#585=LINE('',#8257,#873);
#586=LINE('',#8259,#874);
#587=LINE('',#8260,#875);
#588=LINE('',#8263,#876);
#589=LINE('',#8265,#877);
#590=LINE('',#8266,#878);
#591=LINE('',#8269,#879);
#592=LINE('',#8271,#880);
#593=LINE('',#8272,#881);
#594=LINE('',#8275,#882);
#595=LINE('',#8277,#883);
#596=LINE('',#8278,#884);
#597=LINE('',#8280,#885);
#598=LINE('',#8281,#886);
#863=VECTOR('',#6644,0.625);
#864=VECTOR('',#6649,0.65);
#865=VECTOR('',#6654,0.635);
#866=VECTOR('',#6663,0.41);
#867=VECTOR('',#6668,0.4);
#868=VECTOR('',#6673,0.36);
#869=VECTOR('',#6678,1.);
#870=VECTOR('',#6679,1.);
#871=VECTOR('',#6680,1.);
#872=VECTOR('',#6681,1.);
#873=VECTOR('',#6684,1.);
#874=VECTOR('',#6685,1.);
#875=VECTOR('',#6686,1.);
#876=VECTOR('',#6689,1.);
#877=VECTOR('',#6690,1.);
#878=VECTOR('',#6691,1.);
#879=VECTOR('',#6694,1.);
#880=VECTOR('',#6695,1.);
#881=VECTOR('',#6696,1.);
#882=VECTOR('',#6699,1.);
#883=VECTOR('',#6700,1.);
#884=VECTOR('',#6701,1.);
#885=VECTOR('',#6704,1.);
#886=VECTOR('',#6705,1.);
#1054=CYLINDRICAL_SURFACE('',#5541,0.65);
#1055=CYLINDRICAL_SURFACE('',#5549,0.3933);
#1165=FACE_BOUND('',#1705,.T.);
#1353=FACE_OUTER_BOUND('',#1700,.T.);
#1354=FACE_OUTER_BOUND('',#1701,.T.);
#1355=FACE_OUTER_BOUND('',#1702,.T.);
#1356=FACE_OUTER_BOUND('',#1703,.T.);
#1357=FACE_OUTER_BOUND('',#1704,.T.);
#1358=FACE_OUTER_BOUND('',#1706,.T.);
#1359=FACE_OUTER_BOUND('',#1707,.T.);
#1360=FACE_OUTER_BOUND('',#1708,.T.);
#1361=FACE_OUTER_BOUND('',#1709,.T.);
#1362=FACE_OUTER_BOUND('',#1710,.T.);
#1363=FACE_OUTER_BOUND('',#1711,.T.);
#1364=FACE_OUTER_BOUND('',#1712,.T.);
#1365=FACE_OUTER_BOUND('',#1713,.T.);
#1366=FACE_OUTER_BOUND('',#1714,.T.);
#1367=FACE_OUTER_BOUND('',#1715,.T.);
#1368=FACE_OUTER_BOUND('',#1716,.T.);
#1369=FACE_OUTER_BOUND('',#1717,.T.);
#1700=EDGE_LOOP('',(#3814));
#1701=EDGE_LOOP('',(#3815,#3816,#3817,#3818));
#1702=EDGE_LOOP('',(#3819,#3820,#3821,#3822));
#1703=EDGE_LOOP('',(#3823,#3824,#3825,#3826));
#1704=EDGE_LOOP('',(#3827));
#1705=EDGE_LOOP('',(#3828));
#1706=EDGE_LOOP('',(#3829,#3830,#3831,#3832));
#1707=EDGE_LOOP('',(#3833,#3834,#3835,#3836));
#1708=EDGE_LOOP('',(#3837,#3838,#3839,#3840));
#1709=EDGE_LOOP('',(#3841));
#1710=EDGE_LOOP('',(#3842,#3843,#3844,#3845));
#1711=EDGE_LOOP('',(#3846,#3847,#3848,#3849));
#1712=EDGE_LOOP('',(#3850,#3851,#3852,#3853));
#1713=EDGE_LOOP('',(#3854,#3855,#3856,#3857));
#1714=EDGE_LOOP('',(#3858,#3859,#3860,#3861));
#1715=EDGE_LOOP('',(#3862,#3863,#3864,#3865));
#1716=EDGE_LOOP('',(#3866,#3867,#3868,#3869,#3870,#3871));
#1717=EDGE_LOOP('',(#3872,#3873,#3874,#3875,#3876,#3877));
#2044=CIRCLE('',#5538,0.6);
#2045=CIRCLE('',#5540,0.65);
#2046=CIRCLE('',#5542,0.65);
#2047=CIRCLE('',#5544,0.62);
#2048=CIRCLE('',#5546,0.42);
#2049=CIRCLE('',#5548,0.3933);
#2050=CIRCLE('',#5550,0.3933);
#2051=CIRCLE('',#5552,0.32);
#2401=VERTEX_POINT('',#8216);
#2402=VERTEX_POINT('',#8219);
#2403=VERTEX_POINT('',#8223);
#2404=VERTEX_POINT('',#8227);
#2405=VERTEX_POINT('',#8231);
#2406=VERTEX_POINT('',#8234);
#2407=VERTEX_POINT('',#8238);
#2408=VERTEX_POINT('',#8242);
#2409=VERTEX_POINT('',#8247);
#2410=VERTEX_POINT('',#8248);
#2411=VERTEX_POINT('',#8250);
#2412=VERTEX_POINT('',#8252);
#2413=VERTEX_POINT('',#8256);
#2414=VERTEX_POINT('',#8258);
#2415=VERTEX_POINT('',#8262);
#2416=VERTEX_POINT('',#8264);
#2417=VERTEX_POINT('',#8268);
#2418=VERTEX_POINT('',#8270);
#2419=VERTEX_POINT('',#8274);
#2420=VERTEX_POINT('',#8276);
#2911=EDGE_CURVE('',#2401,#2401,#2044,.T.);
#2912=EDGE_CURVE('',#2402,#2402,#2045,.T.);
#2913=EDGE_CURVE('',#2402,#2401,#575,.T.);
#2914=EDGE_CURVE('',#2403,#2403,#2046,.T.);
#2915=EDGE_CURVE('',#2403,#2402,#576,.T.);
#2916=EDGE_CURVE('',#2404,#2404,#2047,.T.);
#2917=EDGE_CURVE('',#2404,#2403,#577,.T.);
#2918=EDGE_CURVE('',#2405,#2405,#2048,.T.);
#2919=EDGE_CURVE('',#2406,#2406,#2049,.F.);
#2920=EDGE_CURVE('',#2406,#2405,#578,.T.);
#2921=EDGE_CURVE('',#2407,#2407,#2050,.F.);
#2922=EDGE_CURVE('',#2407,#2406,#579,.T.);
#2923=EDGE_CURVE('',#2408,#2408,#2051,.T.);
#2924=EDGE_CURVE('',#2408,#2407,#580,.T.);
#2925=EDGE_CURVE('',#2409,#2410,#581,.T.);
#2926=EDGE_CURVE('',#2410,#2411,#582,.T.);
#2927=EDGE_CURVE('',#2411,#2412,#583,.T.);
#2928=EDGE_CURVE('',#2409,#2412,#584,.T.);
#2929=EDGE_CURVE('',#2410,#2413,#585,.T.);
#2930=EDGE_CURVE('',#2413,#2414,#586,.T.);
#2931=EDGE_CURVE('',#2414,#2411,#587,.T.);
#2932=EDGE_CURVE('',#2413,#2415,#588,.T.);
#2933=EDGE_CURVE('',#2415,#2416,#589,.T.);
#2934=EDGE_CURVE('',#2416,#2414,#590,.T.);
#2935=EDGE_CURVE('',#2415,#2417,#591,.T.);
#2936=EDGE_CURVE('',#2417,#2418,#592,.T.);
#2937=EDGE_CURVE('',#2418,#2416,#593,.T.);
#2938=EDGE_CURVE('',#2417,#2419,#594,.T.);
#2939=EDGE_CURVE('',#2419,#2420,#595,.T.);
#2940=EDGE_CURVE('',#2420,#2418,#596,.T.);
#2941=EDGE_CURVE('',#2419,#2409,#597,.T.);
#2942=EDGE_CURVE('',#2412,#2420,#598,.T.);
#3814=ORIENTED_EDGE('',*,*,#2911,.F.);
#3815=ORIENTED_EDGE('',*,*,#2912,.F.);
#3816=ORIENTED_EDGE('',*,*,#2913,.T.);
#3817=ORIENTED_EDGE('',*,*,#2911,.T.);
#3818=ORIENTED_EDGE('',*,*,#2913,.F.);
#3819=ORIENTED_EDGE('',*,*,#2914,.F.);
#3820=ORIENTED_EDGE('',*,*,#2915,.T.);
#3821=ORIENTED_EDGE('',*,*,#2912,.T.);
#3822=ORIENTED_EDGE('',*,*,#2915,.F.);
#3823=ORIENTED_EDGE('',*,*,#2916,.F.);
#3824=ORIENTED_EDGE('',*,*,#2917,.T.);
#3825=ORIENTED_EDGE('',*,*,#2914,.T.);
#3826=ORIENTED_EDGE('',*,*,#2917,.F.);
#3827=ORIENTED_EDGE('',*,*,#2916,.T.);
#3828=ORIENTED_EDGE('',*,*,#2918,.F.);
#3829=ORIENTED_EDGE('',*,*,#2919,.F.);
#3830=ORIENTED_EDGE('',*,*,#2920,.T.);
#3831=ORIENTED_EDGE('',*,*,#2918,.T.);
#3832=ORIENTED_EDGE('',*,*,#2920,.F.);
#3833=ORIENTED_EDGE('',*,*,#2921,.F.);
#3834=ORIENTED_EDGE('',*,*,#2922,.T.);
#3835=ORIENTED_EDGE('',*,*,#2919,.T.);
#3836=ORIENTED_EDGE('',*,*,#2922,.F.);
#3837=ORIENTED_EDGE('',*,*,#2923,.F.);
#3838=ORIENTED_EDGE('',*,*,#2924,.T.);
#3839=ORIENTED_EDGE('',*,*,#2921,.T.);
#3840=ORIENTED_EDGE('',*,*,#2924,.F.);
#3841=ORIENTED_EDGE('',*,*,#2923,.T.);
#3842=ORIENTED_EDGE('',*,*,#2925,.T.);
#3843=ORIENTED_EDGE('',*,*,#2926,.T.);
#3844=ORIENTED_EDGE('',*,*,#2927,.T.);
#3845=ORIENTED_EDGE('',*,*,#2928,.F.);
#3846=ORIENTED_EDGE('',*,*,#2929,.T.);
#3847=ORIENTED_EDGE('',*,*,#2930,.T.);
#3848=ORIENTED_EDGE('',*,*,#2931,.T.);
#3849=ORIENTED_EDGE('',*,*,#2926,.F.);
#3850=ORIENTED_EDGE('',*,*,#2932,.T.);
#3851=ORIENTED_EDGE('',*,*,#2933,.T.);
#3852=ORIENTED_EDGE('',*,*,#2934,.T.);
#3853=ORIENTED_EDGE('',*,*,#2930,.F.);
#3854=ORIENTED_EDGE('',*,*,#2935,.T.);
#3855=ORIENTED_EDGE('',*,*,#2936,.T.);
#3856=ORIENTED_EDGE('',*,*,#2937,.T.);
#3857=ORIENTED_EDGE('',*,*,#2933,.F.);
#3858=ORIENTED_EDGE('',*,*,#2938,.T.);
#3859=ORIENTED_EDGE('',*,*,#2939,.T.);
#3860=ORIENTED_EDGE('',*,*,#2940,.T.);
#3861=ORIENTED_EDGE('',*,*,#2936,.F.);
#3862=ORIENTED_EDGE('',*,*,#2941,.T.);
#3863=ORIENTED_EDGE('',*,*,#2928,.T.);
#3864=ORIENTED_EDGE('',*,*,#2942,.T.);
#3865=ORIENTED_EDGE('',*,*,#2939,.F.);
#3866=ORIENTED_EDGE('',*,*,#2941,.F.);
#3867=ORIENTED_EDGE('',*,*,#2938,.F.);
#3868=ORIENTED_EDGE('',*,*,#2935,.F.);
#3869=ORIENTED_EDGE('',*,*,#2932,.F.);
#3870=ORIENTED_EDGE('',*,*,#2929,.F.);
#3871=ORIENTED_EDGE('',*,*,#2925,.F.);
#3872=ORIENTED_EDGE('',*,*,#2942,.F.);
#3873=ORIENTED_EDGE('',*,*,#2927,.F.);
#3874=ORIENTED_EDGE('',*,*,#2931,.F.);
#3875=ORIENTED_EDGE('',*,*,#2934,.F.);
#3876=ORIENTED_EDGE('',*,*,#2937,.F.);
#3877=ORIENTED_EDGE('',*,*,#2940,.F.);
#4524=PLANE('',#5537);
#4525=PLANE('',#5545);
#4526=PLANE('',#5553);
#4527=PLANE('',#5554);
#4528=PLANE('',#5555);
#4529=PLANE('',#5556);
#4530=PLANE('',#5557);
#4531=PLANE('',#5558);
#4532=PLANE('',#5559);
#4533=PLANE('',#5560);
#4534=PLANE('',#5561);
#4729=ADVANCED_FACE('',(#1353),#4524,.T.);
#4730=ADVANCED_FACE('',(#1354),#272,.T.);
#4731=ADVANCED_FACE('',(#1355),#1054,.T.);
#4732=ADVANCED_FACE('',(#1356),#273,.T.);
#4733=ADVANCED_FACE('',(#1357,#1165),#4525,.T.);
#4734=ADVANCED_FACE('',(#1358),#274,.T.);
#4735=ADVANCED_FACE('',(#1359),#1055,.T.);
#4736=ADVANCED_FACE('',(#1360),#275,.T.);
#4737=ADVANCED_FACE('',(#1361),#4526,.T.);
#4738=ADVANCED_FACE('',(#1362),#4527,.F.);
#4739=ADVANCED_FACE('',(#1363),#4528,.F.);
#4740=ADVANCED_FACE('',(#1364),#4529,.F.);
#4741=ADVANCED_FACE('',(#1365),#4530,.F.);
#4742=ADVANCED_FACE('',(#1366),#4531,.F.);
#4743=ADVANCED_FACE('',(#1367),#4532,.F.);
#4744=ADVANCED_FACE('',(#1368),#4533,.F.);
#4745=ADVANCED_FACE('',(#1369),#4534,.F.);
#4903=CLOSED_SHELL('',(#4729,#4730,#4731,#4732,#4733,#4734,#4735,#4736,
#4737));
#4904=CLOSED_SHELL('',(#4738,#4739,#4740,#4741,#4742,#4743,#4744,#4745));
#5536=AXIS2_PLACEMENT_3D('',#8214,#6634,#6635);
#5537=AXIS2_PLACEMENT_3D('',#8215,#6636,#6637);
#5538=AXIS2_PLACEMENT_3D('',#8217,#6638,#6639);
#5539=AXIS2_PLACEMENT_3D('',#8218,#6640,#6641);
#5540=AXIS2_PLACEMENT_3D('',#8220,#6642,#6643);
#5541=AXIS2_PLACEMENT_3D('',#8222,#6645,#6646);
#5542=AXIS2_PLACEMENT_3D('',#8224,#6647,#6648);
#5543=AXIS2_PLACEMENT_3D('',#8226,#6650,#6651);
#5544=AXIS2_PLACEMENT_3D('',#8228,#6652,#6653);
#5545=AXIS2_PLACEMENT_3D('',#8230,#6655,#6656);
#5546=AXIS2_PLACEMENT_3D('',#8232,#6657,#6658);
#5547=AXIS2_PLACEMENT_3D('',#8233,#6659,#6660);
#5548=AXIS2_PLACEMENT_3D('',#8235,#6661,#6662);
#5549=AXIS2_PLACEMENT_3D('',#8237,#6664,#6665);
#5550=AXIS2_PLACEMENT_3D('',#8239,#6666,#6667);
#5551=AXIS2_PLACEMENT_3D('',#8241,#6669,#6670);
#5552=AXIS2_PLACEMENT_3D('',#8243,#6671,#6672);
#5553=AXIS2_PLACEMENT_3D('',#8245,#6674,#6675);
#5554=AXIS2_PLACEMENT_3D('',#8246,#6676,#6677);
#5555=AXIS2_PLACEMENT_3D('',#8255,#6682,#6683);
#5556=AXIS2_PLACEMENT_3D('',#8261,#6687,#6688);
#5557=AXIS2_PLACEMENT_3D('',#8267,#6692,#6693);
#5558=AXIS2_PLACEMENT_3D('',#8273,#6697,#6698);
#5559=AXIS2_PLACEMENT_3D('',#8279,#6702,#6703);
#5560=AXIS2_PLACEMENT_3D('',#8282,#6706,#6707);
#5561=AXIS2_PLACEMENT_3D('',#8283,#6708,#6709);
#6634=DIRECTION('axis',(0.,0.,1.));
#6635=DIRECTION('refdir',(1.,0.,0.));
#6636=DIRECTION('center_axis',(0.,1.,0.));
#6637=DIRECTION('ref_axis',(0.,0.,1.));
#6638=DIRECTION('center_axis',(0.,-1.,0.));
#6639=DIRECTION('ref_axis',(1.,0.,0.));
#6640=DIRECTION('center_axis',(0.,-1.,0.));
#6641=DIRECTION('ref_axis',(1.,0.,0.));
#6642=DIRECTION('center_axis',(0.,-1.,0.));
#6643=DIRECTION('ref_axis',(1.,0.,0.));
#6644=DIRECTION('',(0.707106781186548,0.707106781186547,8.65956056235493E-17));
#6645=DIRECTION('center_axis',(0.,-1.,0.));
#6646=DIRECTION('ref_axis',(1.,0.,0.));
#6647=DIRECTION('center_axis',(0.,-1.,0.));
#6648=DIRECTION('ref_axis',(1.,0.,0.));
#6649=DIRECTION('',(0.,1.,0.));
#6650=DIRECTION('center_axis',(0.,1.,0.));
#6651=DIRECTION('ref_axis',(1.,0.,0.));
#6652=DIRECTION('center_axis',(0.,-1.,0.));
#6653=DIRECTION('ref_axis',(1.,0.,0.));
#6654=DIRECTION('',(-0.707106781186548,0.707106781186547,-8.65956056235494E-17));
#6655=DIRECTION('center_axis',(0.,-1.,0.));
#6656=DIRECTION('ref_axis',(0.,0.,-1.));
#6657=DIRECTION('center_axis',(0.,-1.,0.));
#6658=DIRECTION('ref_axis',(1.,0.,0.));
#6659=DIRECTION('center_axis',(0.,1.,0.));
#6660=DIRECTION('ref_axis',(1.,0.,0.));
#6661=DIRECTION('center_axis',(0.,1.,0.));
#6662=DIRECTION('ref_axis',(1.,0.,0.));
#6663=DIRECTION('',(-0.447213595499958,0.894427190999916,-5.47678698264203E-17));
#6664=DIRECTION('center_axis',(0.,-1.,0.));
#6665=DIRECTION('ref_axis',(1.,0.,0.));
#6666=DIRECTION('center_axis',(0.,1.,0.));
#6667=DIRECTION('ref_axis',(1.,0.,0.));
#6668=DIRECTION('',(0.,1.,0.));
#6669=DIRECTION('center_axis',(0.,1.,0.));
#6670=DIRECTION('ref_axis',(1.,0.,0.));
#6671=DIRECTION('center_axis',(0.,-1.,0.));
#6672=DIRECTION('ref_axis',(1.,0.,0.));
#6673=DIRECTION('',(-0.707106781186547,0.707106781186548,-8.65956056235493E-17));
#6674=DIRECTION('center_axis',(0.,-1.,0.));
#6675=DIRECTION('ref_axis',(0.,0.,-1.));
#6676=DIRECTION('center_axis',(0.866025403784439,0.,-0.5));
#6677=DIRECTION('ref_axis',(0.5,0.,0.866025403784439));
#6678=DIRECTION('',(-0.5,0.,-0.866025403784439));
#6679=DIRECTION('',(0.,-1.,0.));
#6680=DIRECTION('',(0.5,0.,0.866025403784439));
#6681=DIRECTION('',(0.,-1.,0.));
#6682=DIRECTION('center_axis',(1.60246890531964E-16,0.,-1.));
#6683=DIRECTION('ref_axis',(1.,0.,1.60246890531964E-16));
#6684=DIRECTION('',(-1.,0.,-1.60246890531964E-16));
#6685=DIRECTION('',(0.,-1.,0.));
#6686=DIRECTION('',(1.,0.,1.60246890531964E-16));
#6687=DIRECTION('center_axis',(-0.866025403784439,0.,-0.5));
#6688=DIRECTION('ref_axis',(0.5,0.,-0.866025403784439));
#6689=DIRECTION('',(-0.5,0.,0.866025403784439));
#6690=DIRECTION('',(0.,-1.,0.));
#6691=DIRECTION('',(0.5,0.,-0.866025403784439));
#6692=DIRECTION('center_axis',(-0.866025403784439,0.,0.5));
#6693=DIRECTION('ref_axis',(-0.5,0.,-0.866025403784439));
#6694=DIRECTION('',(0.5,0.,0.866025403784439));
#6695=DIRECTION('',(0.,-1.,0.));
#6696=DIRECTION('',(-0.5,0.,-0.866025403784439));
#6697=DIRECTION('center_axis',(-1.60246890531964E-16,0.,1.));
#6698=DIRECTION('ref_axis',(-1.,0.,-1.60246890531964E-16));
#6699=DIRECTION('',(1.,0.,1.60246890531964E-16));
#6700=DIRECTION('',(0.,-1.,0.));
#6701=DIRECTION('',(-1.,0.,-1.60246890531964E-16));
#6702=DIRECTION('center_axis',(0.866025403784439,0.,0.5));
#6703=DIRECTION('ref_axis',(-0.5,0.,0.866025403784439));
#6704=DIRECTION('',(0.5,0.,-0.866025403784439));
#6705=DIRECTION('',(-0.5,0.,0.866025403784439));
#6706=DIRECTION('center_axis',(0.,1.,0.));
#6707=DIRECTION('ref_axis',(1.,0.,0.));
#6708=DIRECTION('center_axis',(0.,-1.,0.));
#6709=DIRECTION('ref_axis',(0.,0.,-1.));
#8214=CARTESIAN_POINT('',(0.,0.,0.));
#8215=CARTESIAN_POINT('Origin',(0.6,0.8,0.));
#8216=CARTESIAN_POINT('',(-0.6,0.8,-7.34788079488412E-17));
#8217=CARTESIAN_POINT('Origin',(0.,0.8,0.));
#8218=CARTESIAN_POINT('Origin',(0.,0.775,0.));
#8219=CARTESIAN_POINT('',(-0.65,0.75,-7.9602041944578E-17));
#8220=CARTESIAN_POINT('Origin',(0.,0.75,0.));
#8221=CARTESIAN_POINT('',(-0.625,0.775,-7.65404249467096E-17));
#8222=CARTESIAN_POINT('Origin',(0.,0.39,0.));
#8223=CARTESIAN_POINT('',(-0.65,0.0299999999999998,-7.9602041944578E-17));
#8224=CARTESIAN_POINT('Origin',(0.,0.0299999999999998,0.));
#8225=CARTESIAN_POINT('',(-0.65,0.39,-7.9602041944578E-17));
#8226=CARTESIAN_POINT('Origin',(0.,0.0150000000000001,0.));
#8227=CARTESIAN_POINT('',(-0.62,5.89805981832114E-17,-7.59281015471359E-17));
#8228=CARTESIAN_POINT('Origin',(0.,0.,0.));
#8229=CARTESIAN_POINT('',(-0.635,0.0150000000000001,-7.77650717458569E-17));
#8230=CARTESIAN_POINT('Origin',(0.42,0.,0.));
#8231=CARTESIAN_POINT('',(-0.42,-3.46944695195361E-18,-5.14351655641888E-17));
#8232=CARTESIAN_POINT('Origin',(0.,0.,0.));
#8233=CARTESIAN_POINT('Origin',(0.,-0.02,0.));
#8234=CARTESIAN_POINT('',(-0.3933,-0.0534000000000001,4.81653586104654E-17));
#8235=CARTESIAN_POINT('Origin',(0.,-0.0534000000000001,0.));
#8236=CARTESIAN_POINT('',(-0.41,-0.02,-5.02105187650415E-17));
#8237=CARTESIAN_POINT('Origin',(0.,-1.48,0.));
#8238=CARTESIAN_POINT('',(-0.3933,-2.9267,4.81653586104654E-17));
#8239=CARTESIAN_POINT('Origin',(0.,-2.9267,0.));
#8240=CARTESIAN_POINT('',(-0.3933,-1.48,-4.81653586104654E-17));
#8241=CARTESIAN_POINT('Origin',(0.,-2.96,0.));
#8242=CARTESIAN_POINT('',(-0.32,-3.,-3.91886975727153E-17));
#8243=CARTESIAN_POINT('Origin',(0.,-3.,0.));
#8244=CARTESIAN_POINT('',(-0.36,-2.96,-4.40872847693047E-17));
#8245=CARTESIAN_POINT('Origin',(0.,-3.,0.));
#8246=CARTESIAN_POINT('Origin',(0.173205080756888,-0.8,-0.3));
#8247=CARTESIAN_POINT('',(0.346410161513775,-0.8,0.));
#8248=CARTESIAN_POINT('',(0.173205080756888,-0.8,-0.3));
#8249=CARTESIAN_POINT('',(0.346410161513775,-0.8,0.));
#8250=CARTESIAN_POINT('',(0.173205080756888,-1.28,-0.3));
#8251=CARTESIAN_POINT('',(0.173205080756888,-0.8,-0.3));
#8252=CARTESIAN_POINT('',(0.346410161513775,-1.28,0.));
#8253=CARTESIAN_POINT('',(0.346410161513775,-1.28,0.));
#8254=CARTESIAN_POINT('',(0.346410161513775,-0.8,0.));
#8255=CARTESIAN_POINT('Origin',(-0.173205080756888,-0.8,-0.3));
#8256=CARTESIAN_POINT('',(-0.173205080756888,-0.8,-0.3));
#8257=CARTESIAN_POINT('',(0.173205080756888,-0.8,-0.3));
#8258=CARTESIAN_POINT('',(-0.173205080756888,-1.28,-0.3));
#8259=CARTESIAN_POINT('',(-0.173205080756888,-0.8,-0.3));
#8260=CARTESIAN_POINT('',(0.173205080756888,-1.28,-0.3));
#8261=CARTESIAN_POINT('Origin',(-0.346410161513775,-0.8,-5.55111512312578E-17));
#8262=CARTESIAN_POINT('',(-0.346410161513775,-0.8,-4.24230095489963E-17));
#8263=CARTESIAN_POINT('',(-0.173205080756888,-0.8,-0.3));
#8264=CARTESIAN_POINT('',(-0.346410161513775,-1.28,-5.55111512312578E-17));
#8265=CARTESIAN_POINT('',(-0.346410161513775,-0.8,-4.24230095489963E-17));
#8266=CARTESIAN_POINT('',(-0.173205080756888,-1.28,-0.3));
#8267=CARTESIAN_POINT('Origin',(-0.173205080756888,-0.8,0.3));
#8268=CARTESIAN_POINT('',(-0.173205080756888,-0.8,0.3));
#8269=CARTESIAN_POINT('',(-0.346410161513775,-0.8,-4.24230095489963E-17));
#8270=CARTESIAN_POINT('',(-0.173205080756888,-1.28,0.3));
#8271=CARTESIAN_POINT('',(-0.173205080756888,-0.8,0.3));
#8272=CARTESIAN_POINT('',(-0.346410161513775,-1.28,-4.24230095489963E-17));
#8273=CARTESIAN_POINT('Origin',(0.173205080756888,-0.8,0.3));
#8274=CARTESIAN_POINT('',(0.173205080756888,-0.8,0.3));
#8275=CARTESIAN_POINT('',(-0.173205080756888,-0.8,0.3));
#8276=CARTESIAN_POINT('',(0.173205080756888,-1.28,0.3));
#8277=CARTESIAN_POINT('',(0.173205080756888,-0.8,0.3));
#8278=CARTESIAN_POINT('',(-0.173205080756888,-1.28,0.3));
#8279=CARTESIAN_POINT('Origin',(0.346410161513775,-0.8,0.));
#8280=CARTESIAN_POINT('',(0.173205080756888,-0.8,0.3));
#8281=CARTESIAN_POINT('',(0.173205080756888,-1.28,0.3));
#8282=CARTESIAN_POINT('Origin',(0.,-0.8,-5.55111512312578E-17));
#8283=CARTESIAN_POINT('Origin',(0.,-1.28,-5.55111512312578E-17));
#9335=UNCERTAINTY_MEASURE_WITH_UNIT(LENGTH_MEASURE(0.001),#9392,
'DISTANCE_ACCURACY_VALUE',
'Maximum model space distance between geometric entities at asserted c
onnectivities');
#9354=UNCERTAINTY_MEASURE_WITH_UNIT(LENGTH_MEASURE(0.001),#9392,
'DISTANCE_ACCURACY_VALUE',
'Maximum model space distance between geometric entities at asserted c
onnectivities');
#9372=(
GEOMETRIC_REPRESENTATION_CONTEXT(3)
GLOBAL_UNCERTAINTY_ASSIGNED_CONTEXT((#9335))
GLOBAL_UNIT_ASSIGNED_CONTEXT((#9392,#9394,#9395))
REPRESENTATION_CONTEXT('','3D')
);
#9391=(
GEOMETRIC_REPRESENTATION_CONTEXT(3)
GLOBAL_UNCERTAINTY_ASSIGNED_CONTEXT((#9354))
GLOBAL_UNIT_ASSIGNED_CONTEXT((#9392,#9394,#9395))
REPRESENTATION_CONTEXT('','3D')
);
#9392=(
LENGTH_UNIT()
NAMED_UNIT(*)
SI_UNIT(.CENTI.,.METRE.)
);
#9394=(
NAMED_UNIT(*)
PLANE_ANGLE_UNIT()
SI_UNIT($,.RADIAN.)
);
#9395=(
NAMED_UNIT(*)
SI_UNIT($,.STERADIAN.)
SOLID_ANGLE_UNIT()
);
#9413=SHAPE_DEFINITION_REPRESENTATION(#9449,#9537);
#9449=PRODUCT_DEFINITION_SHAPE('',$,#9574);
#9537=SHAPE_REPRESENTATION('',(#5536),#9372);
#9556=PRODUCT_DEFINITION_CONTEXT('part definition',#9666,'design');
#9574=PRODUCT_DEFINITION('Cap Screw - M8x30','Cap Screw - M8x30',#9610,
#9556);
#9610=PRODUCT_DEFINITION_FORMATION('',$,#9685);
#9666=APPLICATION_CONTEXT(
'Core Data for Automotive Mechanical Design Process');
#9667=PRODUCT_CONTEXT('part definition',#9666,'mechanical');
#9685=PRODUCT('Cap Screw - M8x30','Cap Screw - M8x30',
'Cap Screw - M8x30',(#9667));
#9760=COLOUR_RGB('Black',0.12,0.14,0.17);
#9761=FILL_AREA_STYLE_COLOUR('',#9760);
#9762=FILL_AREA_STYLE('',(#9761));
#9763=SURFACE_STYLE_FILL_AREA(#9762);
#9764=SURFACE_SIDE_STYLE('',(#9763));
#9765=SURFACE_STYLE_USAGE(.BOTH.,#9764);
#9766=PRESENTATION_STYLE_ASSIGNMENT((#9765));
ENDSEC;
END-ISO-10303-21;
